ISO-10303-21;
HEADER;
/* Generated by software containing ST-Developer
 * from STEP Tools, Inc. (www.steptools.com) 
 */

FILE_DESCRIPTION(
/* description */ ('Hand-crank flanged shaft unit'),
/* implementation_level */ '2;1');

FILE_NAME(
/* name */ 'Socket Set Screw - M6x8.step',
/* time_stamp */ '2026-10-27T18:35:45-07:00',
/* author */ (''),
/* organization */ (''),
/* preprocessor_version */ 'ST-DEVELOPER v20.2',
/* originating_system */ 'Autodesk Translation Framework v15.17.0.0',
/* authorisation */ '');

FILE_SCHEMA (('AUTOMOTIVE_DESIGN { 1 0 10303 214 3 1 1 }'));
ENDSEC;

DATA;
#10=MECHANICAL_DESIGN_GEOMETRIC_PRESENTATION_REPRESENTATION('',(#297),#6805);
#22=CONICAL_SURFACE('',#3888,0.285,0.785398163397448);
#23=CONICAL_SURFACE('',#3892,0.25,0.785398163397448);
#256=SHAPE_REPRESENTATION_RELATIONSHIP('SRR','None',#6919,#276);
#276=ADVANCED_BREP_SHAPE_REPRESENTATION('',(#317),#6802);
#297=STYLED_ITEM('',(#7098),#317);
#317=MANIFOLD_SOLID_BREP('Body1',#3339);
#404=FACE_BOUND('',#952,.T.);
#495=PLANE('',#3879);
#496=PLANE('',#3880);
#497=PLANE('',#3881);
#498=PLANE('',#3882);
#499=PLANE('',#3883);
#500=PLANE('',#3884);
#501=PLANE('',#3885);
#502=PLANE('',#3886);
#503=PLANE('',#3894);
#672=FACE_OUTER_BOUND('',#944,.T.);
#673=FACE_OUTER_BOUND('',#945,.T.);
#674=FACE_OUTER_BOUND('',#946,.T.);
#675=FACE_OUTER_BOUND('',#947,.T.);
#676=FACE_OUTER_BOUND('',#948,.T.);
#677=FACE_OUTER_BOUND('',#949,.T.);
#678=FACE_OUTER_BOUND('',#950,.T.);
#679=FACE_OUTER_BOUND('',#951,.T.);
#680=FACE_OUTER_BOUND('',#953,.T.);
#681=FACE_OUTER_BOUND('',#954,.T.);
#682=FACE_OUTER_BOUND('',#955,.T.);
#683=FACE_OUTER_BOUND('',#956,.T.);
#944=EDGE_LOOP('',(#2941,#2942,#2943,#2944));
#945=EDGE_LOOP('',(#2945,#2946,#2947,#2948));
#946=EDGE_LOOP('',(#2949,#2950,#2951,#2952));
#947=EDGE_LOOP('',(#2953,#2954,#2955,#2956));
#948=EDGE_LOOP('',(#2957,#2958,#2959,#2960));
#949=EDGE_LOOP('',(#2961,#2962,#2963,#2964));
#950=EDGE_LOOP('',(#2965,#2966,#2967,#2968,#2969,#2970));
#951=EDGE_LOOP('',(#2971));
#952=EDGE_LOOP('',(#2972,#2973,#2974,#2975,#2976,#2977));
#953=EDGE_LOOP('',(#2978,#2979,#2980,#2981));
#954=EDGE_LOOP('',(#2982,#2983,#2984,#2985));
#955=EDGE_LOOP('',(#2986,#2987,#2988,#2989));
#956=EDGE_LOOP('',(#2990));
#1162=LINE('',#6547,#1390);
#1163=LINE('',#6549,#1391);
#1164=LINE('',#6551,#1392);
#1165=LINE('',#6552,#1393);
#1166=LINE('',#6555,#1394);
#1167=LINE('',#6557,#1395);
#1168=LINE('',#6558,#1396);
#1169=LINE('',#6561,#1397);
#1170=LINE('',#6563,#1398);
#1171=LINE('',#6564,#1399);
#1172=LINE('',#6567,#1400);
#1173=LINE('',#6569,#1401);
#1174=LINE('',#6570,#1402);
#1175=LINE('',#6573,#1403);
#1176=LINE('',#6575,#1404);
#1177=LINE('',#6576,#1405);
#1178=LINE('',#6578,#1406);
#1179=LINE('',#6579,#1407);
#1180=LINE('',#6587,#1408);
#1181=LINE('',#6591,#1409);
#1182=LINE('',#6595,#1410);
#1390=VECTOR('',#4773,1.);
#1391=VECTOR('',#4774,1.);
#1392=VECTOR('',#4775,1.);
#1393=VECTOR('',#4776,1.);
#1394=VECTOR('',#4779,1.);
#1395=VECTOR('',#4780,1.);
#1396=VECTOR('',#4781,1.);
#1397=VECTOR('',#4784,1.);
#1398=VECTOR('',#4785,1.);
#1399=VECTOR('',#4786,1.);
#1400=VECTOR('',#4789,1.);
#1401=VECTOR('',#4790,1.);
#1402=VECTOR('',#4791,1.);
#1403=VECTOR('',#4794,1.);
#1404=VECTOR('',#4795,1.);
#1405=VECTOR('',#4796,1.);
#1406=VECTOR('',#4799,1.);
#1407=VECTOR('',#4800,1.);
#1408=VECTOR('',#4811,0.285);
#1409=VECTOR('',#4816,0.3);
#1410=VECTOR('',#4821,0.25);
#1555=CIRCLE('',#3887,0.27);
#1556=CIRCLE('',#3889,0.2942);
#1557=CIRCLE('',#3891,0.2942);
#1558=CIRCLE('',#3893,0.2);
#1803=VERTEX_POINT('',#6545);
#1804=VERTEX_POINT('',#6546);
#1805=VERTEX_POINT('',#6548);
#1806=VERTEX_POINT('',#6550);
#1807=VERTEX_POINT('',#6554);
#1808=VERTEX_POINT('',#6556);
#1809=VERTEX_POINT('',#6560);
#1810=VERTEX_POINT('',#6562);
#1811=VERTEX_POINT('',#6566);
#1812=VERTEX_POINT('',#6568);
#1813=VERTEX_POINT('',#6572);
#1814=VERTEX_POINT('',#6574);
#1815=VERTEX_POINT('',#6582);
#1816=VERTEX_POINT('',#6585);
#1817=VERTEX_POINT('',#6589);
#1818=VERTEX_POINT('',#6593);
#2188=EDGE_CURVE('',#1803,#1804,#1162,.T.);
#2189=EDGE_CURVE('',#1803,#1805,#1163,.T.);
#2190=EDGE_CURVE('',#1805,#1806,#1164,.T.);
#2191=EDGE_CURVE('',#1804,#1806,#1165,.T.);
#2192=EDGE_CURVE('',#1807,#1803,#1166,.T.);
#2193=EDGE_CURVE('',#1807,#1808,#1167,.T.);
#2194=EDGE_CURVE('',#1808,#1805,#1168,.T.);
#2195=EDGE_CURVE('',#1809,#1807,#1169,.T.);
#2196=EDGE_CURVE('',#1809,#1810,#1170,.T.);
#2197=EDGE_CURVE('',#1810,#1808,#1171,.T.);
#2198=EDGE_CURVE('',#1811,#1809,#1172,.T.);
#2199=EDGE_CURVE('',#1811,#1812,#1173,.T.);
#2200=EDGE_CURVE('',#1812,#1810,#1174,.T.);
#2201=EDGE_CURVE('',#1813,#1811,#1175,.T.);
#2202=EDGE_CURVE('',#1813,#1814,#1176,.T.);
#2203=EDGE_CURVE('',#1814,#1812,#1177,.T.);
#2204=EDGE_CURVE('',#1804,#1813,#1178,.T.);
#2205=EDGE_CURVE('',#1806,#1814,#1179,.T.);
#2206=EDGE_CURVE('',#1815,#1815,#1555,.T.);
#2207=EDGE_CURVE('',#1816,#1816,#1556,.T.);
#2208=EDGE_CURVE('',#1816,#1815,#1180,.T.);
#2209=EDGE_CURVE('',#1817,#1817,#1557,.F.);
#2210=EDGE_CURVE('',#1817,#1816,#1181,.T.);
#2211=EDGE_CURVE('',#1818,#1818,#1558,.T.);
#2212=EDGE_CURVE('',#1818,#1817,#1182,.T.);
#2941=ORIENTED_EDGE('',*,*,#2188,.F.);
#2942=ORIENTED_EDGE('',*,*,#2189,.T.);
#2943=ORIENTED_EDGE('',*,*,#2190,.T.);
#2944=ORIENTED_EDGE('',*,*,#2191,.F.);
#2945=ORIENTED_EDGE('',*,*,#2192,.F.);
#2946=ORIENTED_EDGE('',*,*,#2193,.T.);
#2947=ORIENTED_EDGE('',*,*,#2194,.T.);
#2948=ORIENTED_EDGE('',*,*,#2189,.F.);
#2949=ORIENTED_EDGE('',*,*,#2195,.F.);
#2950=ORIENTED_EDGE('',*,*,#2196,.T.);
#2951=ORIENTED_EDGE('',*,*,#2197,.T.);
#2952=ORIENTED_EDGE('',*,*,#2193,.F.);
#2953=ORIENTED_EDGE('',*,*,#2198,.F.);
#2954=ORIENTED_EDGE('',*,*,#2199,.T.);
#2955=ORIENTED_EDGE('',*,*,#2200,.T.);
#2956=ORIENTED_EDGE('',*,*,#2196,.F.);
#2957=ORIENTED_EDGE('',*,*,#2201,.F.);
#2958=ORIENTED_EDGE('',*,*,#2202,.T.);
#2959=ORIENTED_EDGE('',*,*,#2203,.T.);
#2960=ORIENTED_EDGE('',*,*,#2199,.F.);
#2961=ORIENTED_EDGE('',*,*,#2204,.F.);
#2962=ORIENTED_EDGE('',*,*,#2191,.T.);
#2963=ORIENTED_EDGE('',*,*,#2205,.T.);
#2964=ORIENTED_EDGE('',*,*,#2202,.F.);
#2965=ORIENTED_EDGE('',*,*,#2205,.F.);
#2966=ORIENTED_EDGE('',*,*,#2190,.F.);
#2967=ORIENTED_EDGE('',*,*,#2194,.F.);
#2968=ORIENTED_EDGE('',*,*,#2197,.F.);
#2969=ORIENTED_EDGE('',*,*,#2200,.F.);
#2970=ORIENTED_EDGE('',*,*,#2203,.F.);
#2971=ORIENTED_EDGE('',*,*,#2206,.F.);
#2972=ORIENTED_EDGE('',*,*,#2188,.T.);
#2973=ORIENTED_EDGE('',*,*,#2204,.T.);
#2974=ORIENTED_EDGE('',*,*,#2201,.T.);
#2975=ORIENTED_EDGE('',*,*,#2198,.T.);
#2976=ORIENTED_EDGE('',*,*,#2195,.T.);
#2977=ORIENTED_EDGE('',*,*,#2192,.T.);
#2978=ORIENTED_EDGE('',*,*,#2207,.F.);
#2979=ORIENTED_EDGE('',*,*,#2208,.T.);
#2980=ORIENTED_EDGE('',*,*,#2206,.T.);
#2981=ORIENTED_EDGE('',*,*,#2208,.F.);
#2982=ORIENTED_EDGE('',*,*,#2209,.F.);
#2983=ORIENTED_EDGE('',*,*,#2210,.T.);
#2984=ORIENTED_EDGE('',*,*,#2207,.T.);
#2985=ORIENTED_EDGE('',*,*,#2210,.F.);
#2986=ORIENTED_EDGE('',*,*,#2211,.F.);
#2987=ORIENTED_EDGE('',*,*,#2212,.T.);
#2988=ORIENTED_EDGE('',*,*,#2209,.T.);
#2989=ORIENTED_EDGE('',*,*,#2212,.F.);
#2990=ORIENTED_EDGE('',*,*,#2211,.T.);
#3127=CYLINDRICAL_SURFACE('',#3890,0.2942);
#3289=ADVANCED_FACE('',(#672),#495,.F.);
#3290=ADVANCED_FACE('',(#673),#496,.F.);
#3291=ADVANCED_FACE('',(#674),#497,.F.);
#3292=ADVANCED_FACE('',(#675),#498,.F.);
#3293=ADVANCED_FACE('',(#676),#499,.F.);
#3294=ADVANCED_FACE('',(#677),#500,.F.);
#3295=ADVANCED_FACE('',(#678),#501,.F.);
#3296=ADVANCED_FACE('',(#679,#404),#502,.T.);
#3297=ADVANCED_FACE('',(#680),#22,.T.);
#3298=ADVANCED_FACE('',(#681),#3127,.T.);
#3299=ADVANCED_FACE('',(#682),#23,.T.);
#3300=ADVANCED_FACE('',(#683),#503,.T.);
#3339=CLOSED_SHELL('',(#3289,#3290,#3291,#3292,#3293,#3294,#3295,#3296,
#3297,#3298,#3299,#3300));
#3878=AXIS2_PLACEMENT_3D('',#6543,#4769,#4770);
#3879=AXIS2_PLACEMENT_3D('',#6544,#4771,#4772);
#3880=AXIS2_PLACEMENT_3D('',#6553,#4777,#4778);
#3881=AXIS2_PLACEMENT_3D('',#6559,#4782,#4783);
#3882=AXIS2_PLACEMENT_3D('',#6565,#4787,#4788);
#3883=AXIS2_PLACEMENT_3D('',#6571,#4792,#4793);
#3884=AXIS2_PLACEMENT_3D('',#6577,#4797,#4798);
#3885=AXIS2_PLACEMENT_3D('',#6580,#4801,#4802);
#3886=AXIS2_PLACEMENT_3D('',#6581,#4803,#4804);
#3887=AXIS2_PLACEMENT_3D('',#6583,#4805,#4806);
#3888=AXIS2_PLACEMENT_3D('',#6584,#4807,#4808);
#3889=AXIS2_PLACEMENT_3D('',#6586,#4809,#4810);
#3890=AXIS2_PLACEMENT_3D('',#6588,#4812,#4813);
#3891=AXIS2_PLACEMENT_3D('',#6590,#4814,#4815);
#3892=AXIS2_PLACEMENT_3D('',#6592,#4817,#4818);
#3893=AXIS2_PLACEMENT_3D('',#6594,#4819,#4820);
#3894=AXIS2_PLACEMENT_3D('',#6596,#4822,#4823);
#4769=DIRECTION('axis',(0.,0.,1.));
#4770=DIRECTION('refdir',(1.,0.,0.));
#4771=DIRECTION('center_axis',(0.866025403784439,0.,-0.5));
#4772=DIRECTION('ref_axis',(0.5,0.,0.866025403784439));
#4773=DIRECTION('',(0.5,0.,0.866025403784439));
#4774=DIRECTION('',(0.,-1.,0.));
#4775=DIRECTION('',(0.5,0.,0.866025403784439));
#4776=DIRECTION('',(0.,-1.,0.));
#4777=DIRECTION('center_axis',(1.60246890531964E-16,0.,-1.));
#4778=DIRECTION('ref_axis',(1.,0.,1.60246890531964E-16));
#4779=DIRECTION('',(1.,0.,1.60246890531964E-16));
#4780=DIRECTION('',(0.,-1.,0.));
#4781=DIRECTION('',(1.,0.,1.60246890531964E-16));
#4782=DIRECTION('center_axis',(-0.866025403784439,0.,-0.5));
#4783=DIRECTION('ref_axis',(0.5,0.,-0.866025403784439));
#4784=DIRECTION('',(0.5,0.,-0.866025403784439));
#4785=DIRECTION('',(0.,-1.,0.));
#4786=DIRECTION('',(0.5,0.,-0.866025403784439));
#4787=DIRECTION('center_axis',(-0.866025403784439,0.,0.5));
#4788=DIRECTION('ref_axis',(-0.5,0.,-0.866025403784439));
#4789=DIRECTION('',(-0.5,0.,-0.866025403784439));
#4790=DIRECTION('',(0.,-1.,0.));
#4791=DIRECTION('',(-0.5,0.,-0.866025403784439));
#4792=DIRECTION('center_axis',(-1.60246890531964E-16,0.,1.));
#4793=DIRECTION('ref_axis',(-1.,0.,-1.60246890531964E-16));
#4794=DIRECTION('',(-1.,0.,-1.60246890531964E-16));
#4795=DIRECTION('',(0.,-1.,0.));
#4796=DIRECTION('',(-1.,0.,-1.60246890531964E-16));
#4797=DIRECTION('center_axis',(0.866025403784439,0.,0.5));
#4798=DIRECTION('ref_axis',(-0.5,0.,0.866025403784439));
#4799=DIRECTION('',(-0.5,0.,0.866025403784439));
#4800=DIRECTION('',(-0.5,0.,0.866025403784439));
#4801=DIRECTION('center_axis',(0.,-1.,0.));
#4802=DIRECTION('ref_axis',(0.,0.,-1.));
#4803=DIRECTION('center_axis',(0.,1.,0.));
#4804=DIRECTION('ref_axis',(0.,0.,1.));
#4805=DIRECTION('center_axis',(0.,-1.,0.));
#4806=DIRECTION('ref_axis',(1.,0.,0.));
#4807=DIRECTION('center_axis',(0.,-1.,0.));
#4808=DIRECTION('ref_axis',(1.,0.,0.));
#4809=DIRECTION('center_axis',(0.,-1.,0.));
#4810=DIRECTION('ref_axis',(1.,0.,0.));
#4811=DIRECTION('',(0.707106781186547,0.707106781186548,8.65956056235493E-17));
#4812=DIRECTION('center_axis',(0.,-1.,0.));
#4813=DIRECTION('ref_axis',(1.,0.,0.));
#4814=DIRECTION('center_axis',(0.,1.,0.));
#4815=DIRECTION('ref_axis',(1.,0.,0.));
#4816=DIRECTION('',(0.,1.,0.));
#4817=DIRECTION('center_axis',(0.,1.,0.));
#4818=DIRECTION('ref_axis',(1.,0.,0.));
#4819=DIRECTION('center_axis',(0.,-1.,0.));
#4820=DIRECTION('ref_axis',(1.,0.,0.));
#4821=DIRECTION('',(-0.707106781186547,0.707106781186548,-8.65956056235493E-17));
#4822=DIRECTION('center_axis',(0.,-1.,0.));
#4823=DIRECTION('ref_axis',(0.,0.,-1.));
#6543=CARTESIAN_POINT('',(0.,0.,0.));
#6544=CARTESIAN_POINT('Origin',(0.0866025403784439,0.,-0.15));
#6545=CARTESIAN_POINT('',(0.0866025403784439,0.,-0.15));
#6546=CARTESIAN_POINT('',(0.173205080756888,0.,0.));
#6547=CARTESIAN_POINT('',(0.142003175473055,0.,-0.0540432852445504));
#6548=CARTESIAN_POINT('',(0.0866025403784439,-0.3,-0.15));
#6549=CARTESIAN_POINT('',(0.0866025403784439,0.,-0.15));
#6550=CARTESIAN_POINT('',(0.173205080756888,-0.3,0.));
#6551=CARTESIAN_POINT('',(0.173205080756888,-0.3,0.));
#6552=CARTESIAN_POINT('',(0.173205080756888,0.,0.));
#6553=CARTESIAN_POINT('Origin',(-0.0866025403784438,0.,-0.15));
#6554=CARTESIAN_POINT('',(-0.0866025403784438,0.,-0.15));
#6555=CARTESIAN_POINT('',(0.0916987298107781,0.,-0.15));
#6556=CARTESIAN_POINT('',(-0.0866025403784438,-0.3,-0.15));
#6557=CARTESIAN_POINT('',(-0.0866025403784438,0.,-0.15));
#6558=CARTESIAN_POINT('',(0.0866025403784439,-0.3,-0.15));
#6559=CARTESIAN_POINT('Origin',(-0.173205080756888,0.,-2.77555756156289E-17));
#6560=CARTESIAN_POINT('',(-0.173205080756888,0.,-2.12115047744981E-17));
#6561=CARTESIAN_POINT('',(-0.117804445662277,0.,-0.0959567147554497));
#6562=CARTESIAN_POINT('',(-0.173205080756888,-0.3,-2.77555756156289E-17));
#6563=CARTESIAN_POINT('',(-0.173205080756888,0.,-2.12115047744981E-17));
#6564=CARTESIAN_POINT('',(-0.0866025403784438,-0.3,-0.15));
#6565=CARTESIAN_POINT('Origin',(-0.0866025403784439,0.,0.15));
#6566=CARTESIAN_POINT('',(-0.0866025403784439,0.,0.15));
#6567=CARTESIAN_POINT('',(-0.074503175473055,0.,0.17095671475545));
#6568=CARTESIAN_POINT('',(-0.0866025403784439,-0.3,0.15));
#6569=CARTESIAN_POINT('',(-0.0866025403784439,0.,0.15));
#6570=CARTESIAN_POINT('',(-0.173205080756888,-0.3,-2.12115047744981E-17));
#6571=CARTESIAN_POINT('Origin',(0.0866025403784439,0.,0.15));
#6572=CARTESIAN_POINT('',(0.0866025403784439,0.,0.15));
#6573=CARTESIAN_POINT('',(0.178301270189222,0.,0.15));
#6574=CARTESIAN_POINT('',(0.0866025403784439,-0.3,0.15));
#6575=CARTESIAN_POINT('',(0.0866025403784439,0.,0.15));
#6576=CARTESIAN_POINT('',(-0.0866025403784439,-0.3,0.15));
#6577=CARTESIAN_POINT('Origin',(0.173205080756888,0.,0.));
#6578=CARTESIAN_POINT('',(0.185304445662277,0.,-0.0209567147554496));
#6579=CARTESIAN_POINT('',(0.0866025403784439,-0.3,0.15));
#6580=CARTESIAN_POINT('Origin',(0.,-0.3,-2.77555756156289E-17));
#6581=CARTESIAN_POINT('Origin',(0.27,0.,0.));
#6582=CARTESIAN_POINT('',(-0.27,5.20417042793042E-18,-3.30654635769785E-17));
#6583=CARTESIAN_POINT('Origin',(0.,0.,0.));
#6584=CARTESIAN_POINT('Origin',(0.,-0.015,0.));
#6585=CARTESIAN_POINT('',(-0.2942,-0.0242,-3.60291088309151E-17));
#6586=CARTESIAN_POINT('Origin',(0.,-0.0242,0.));
#6587=CARTESIAN_POINT('',(-0.285,-0.015,-3.49024337756996E-17));
#6588=CARTESIAN_POINT('Origin',(0.,-0.365,0.));
#6589=CARTESIAN_POINT('',(-0.2942,-0.7058,3.60291088309151E-17));
#6590=CARTESIAN_POINT('Origin',(0.,-0.7058,0.));
#6591=CARTESIAN_POINT('',(-0.2942,-0.365,-3.60291088309151E-17));
#6592=CARTESIAN_POINT('Origin',(0.,-0.75,0.));
#6593=CARTESIAN_POINT('',(-0.2,-0.8,-2.44929359829471E-17));
#6594=CARTESIAN_POINT('Origin',(0.,-0.8,0.));
#6595=CARTESIAN_POINT('',(-0.25,-0.75,-3.06161699786838E-17));
#6596=CARTESIAN_POINT('Origin',(0.,-0.8,0.));
#6777=UNCERTAINTY_MEASURE_WITH_UNIT(LENGTH_MEASURE(0.001),#6806,
'DISTANCE_ACCURACY_VALUE',
'Maximum model space distance between geometric entities at asserted c
onnectivities');
#6780=UNCERTAINTY_MEASURE_WITH_UNIT(LENGTH_MEASURE(0.001),#6806,
'DISTANCE_ACCURACY_VALUE',
'Maximum model space distance between geometric entities at asserted c
onnectivities');
#6802=(
GEOMETRIC_REPRESENTATION_CONTEXT(3)
GLOBAL_UNCERTAINTY_ASSIGNED_CONTEXT((#6777))
GLOBAL_UNIT_ASSIGNED_CONTEXT((#6806,#6808,#6809))
REPRESENTATION_CONTEXT('','3D')
);
#6805=(
GEOMETRIC_REPRESENTATION_CONTEXT(3)
GLOBAL_UNCERTAINTY_ASSIGNED_CONTEXT((#6780))
GLOBAL_UNIT_ASSIGNED_CONTEXT((#6806,#6808,#6809))
REPRESENTATION_CONTEXT('','3D')
);
#6806=(
LENGTH_UNIT()
NAMED_UNIT(*)
SI_UNIT(.CENTI.,.METRE.)
);
#6808=(
NAMED_UNIT(*)
PLANE_ANGLE_UNIT()
SI_UNIT($,.RADIAN.)
);
#6809=(
NAMED_UNIT(*)
SI_UNIT($,.STERADIAN.)
SOLID_ANGLE_UNIT()
);
#6831=SHAPE_DEFINITION_REPRESENTATION(#6885,#6919);
#6885=PRODUCT_DEFINITION_SHAPE('',$,#6944);
#6919=SHAPE_REPRESENTATION('',(#3878),#6802);
#6922=PRODUCT_DEFINITION_CONTEXT('part definition',#6996,'design');
#6944=PRODUCT_DEFINITION('Socket Set Screw - M6x8',
'Socket Set Screw - M6x8',#6968,#6922);
#6968=PRODUCT_DEFINITION_FORMATION('',$,#7019);
#6996=APPLICATION_CONTEXT(
'Core Data for Automotive Mechanical Design Process');
#6997=PRODUCT_CONTEXT('part definition',#6996,'mechanical');
#7019=PRODUCT('Socket Set Screw - M6x8','Socket Set Screw - M6x8',
'Socket Set Screw - M6x8',(#6997));
#7092=COLOUR_RGB('Black',0.12,0.14,0.17);
#7093=FILL_AREA_STYLE_COLOUR('',#7092);
#7094=FILL_AREA_STYLE('',(#7093));
#7095=SURFACE_STYLE_FILL_AREA(#7094);
#7096=SURFACE_SIDE_STYLE('',(#7095));
#7097=SURFACE_STYLE_USAGE(.BOTH.,#7096);
#7098=PRESENTATION_STYLE_ASSIGNMENT((#7097));
ENDSEC;
END-ISO-10303-21;
